ISO-10303-21;
HEADER;
/* Generated by software containing ST-Developer
 * from STEP Tools, Inc. (www.steptools.com) 
 */

FILE_DESCRIPTION(
/* description */ ('PAT-091'),
/* implementation_level */ '2;1');

FILE_NAME(
/* name */ 'Plain pivot bush (8).step',
/* time_stamp */ '2026-10-27T15:34:44-07:00',
/* author */ (''),
/* organization */ (''),
/* preprocessor_version */ 'ST-DEVELOPER v20.2',
/* originating_system */ 'Autodesk Translation Framework v15.17.0.0',
/* authorisation */ '');

FILE_SCHEMA (('AUTOMOTIVE_DESIGN { 1 0 10303 214 3 1 1 }'));
ENDSEC;

DATA;
#10=MECHANICAL_DESIGN_GEOMETRIC_PRESENTATION_REPRESENTATION('',(#1058),#25100);
#838=SHAPE_REPRESENTATION_RELATIONSHIP('SRR','None',#25605,#948);
#948=ADVANCED_BREP_SHAPE_REPRESENTATION('',(#1179),#25075);
#1058=STYLED_ITEM('',(#26177),#1179);
#1179=MANIFOLD_SOLID_BREP('Body1',#13338);
#1585=FACE_BOUND('',#3902,.T.);
#1586=FACE_BOUND('',#3904,.T.);
#1992=PLANE('',#15999);
#1993=PLANE('',#16000);
#2711=FACE_OUTER_BOUND('',#3899,.T.);
#2712=FACE_OUTER_BOUND('',#3900,.T.);
#2713=FACE_OUTER_BOUND('',#3901,.T.);
#2714=FACE_OUTER_BOUND('',#3903,.T.);
#3899=EDGE_LOOP('',(#11516,#11517,#11518,#11519));
#3900=EDGE_LOOP('',(#11520,#11521,#11522,#11523));
#3901=EDGE_LOOP('',(#11524));
#3902=EDGE_LOOP('',(#11525));
#3903=EDGE_LOOP('',(#11526));
#3904=EDGE_LOOP('',(#11527));
#4802=LINE('',#23964,#5542);
#4803=LINE('',#23970,#5543);
#5542=VECTOR('',#19966,0.604999999999997);
#5543=VECTOR('',#19973,1.);
#6194=CIRCLE('',#15994,0.604999999999997);
#6195=CIRCLE('',#15995,0.604999999999997);
#6196=CIRCLE('',#15997,1.);
#6197=CIRCLE('',#15998,1.);
#7227=VERTEX_POINT('',#23961);
#7228=VERTEX_POINT('',#23963);
#7229=VERTEX_POINT('',#23967);
#7230=VERTEX_POINT('',#23969);
#8693=EDGE_CURVE('',#7227,#7227,#6194,.T.);
#8694=EDGE_CURVE('',#7227,#7228,#4802,.T.);
#8695=EDGE_CURVE('',#7228,#7228,#6195,.T.);
#8696=EDGE_CURVE('',#7229,#7229,#6196,.T.);
#8697=EDGE_CURVE('',#7229,#7230,#4803,.T.);
#8698=EDGE_CURVE('',#7230,#7230,#6197,.T.);
#11516=ORIENTED_EDGE('',*,*,#8693,.F.);
#11517=ORIENTED_EDGE('',*,*,#8694,.T.);
#11518=ORIENTED_EDGE('',*,*,#8695,.T.);
#11519=ORIENTED_EDGE('',*,*,#8694,.F.);
#11520=ORIENTED_EDGE('',*,*,#8696,.F.);
#11521=ORIENTED_EDGE('',*,*,#8697,.T.);
#11522=ORIENTED_EDGE('',*,*,#8698,.T.);
#11523=ORIENTED_EDGE('',*,*,#8697,.F.);
#11524=ORIENTED_EDGE('',*,*,#8696,.T.);
#11525=ORIENTED_EDGE('',*,*,#8693,.T.);
#11526=ORIENTED_EDGE('',*,*,#8698,.F.);
#11527=ORIENTED_EDGE('',*,*,#8695,.F.);
#12358=CYLINDRICAL_SURFACE('',#15993,0.604999999999997);
#12359=CYLINDRICAL_SURFACE('',#15996,1.);
#13078=ADVANCED_FACE('',(#2711),#12358,.F.);
#13079=ADVANCED_FACE('',(#2712),#12359,.T.);
#13080=ADVANCED_FACE('',(#2713,#1585),#1992,.T.);
#13081=ADVANCED_FACE('',(#2714,#1586),#1993,.F.);
#13338=CLOSED_SHELL('',(#13078,#13079,#13080,#13081));
#15992=AXIS2_PLACEMENT_3D('',#23959,#19960,#19961);
#15993=AXIS2_PLACEMENT_3D('',#23960,#19962,#19963);
#15994=AXIS2_PLACEMENT_3D('',#23962,#19964,#19965);
#15995=AXIS2_PLACEMENT_3D('',#23965,#19967,#19968);
#15996=AXIS2_PLACEMENT_3D('',#23966,#19969,#19970);
#15997=AXIS2_PLACEMENT_3D('',#23968,#19971,#19972);
#15998=AXIS2_PLACEMENT_3D('',#23971,#19974,#19975);
#15999=AXIS2_PLACEMENT_3D('',#23972,#19976,#19977);
#16000=AXIS2_PLACEMENT_3D('',#23973,#19978,#19979);
#19960=DIRECTION('axis',(0.,0.,1.));
#19961=DIRECTION('refdir',(1.,0.,0.));
#19962=DIRECTION('center_axis',(0.,1.,0.));
#19963=DIRECTION('ref_axis',(1.,0.,0.));
#19964=DIRECTION('center_axis',(0.,-1.,0.));
#19965=DIRECTION('ref_axis',(1.,0.,0.));
#19966=DIRECTION('',(0.,-1.,0.));
#19967=DIRECTION('center_axis',(0.,-1.,0.));
#19968=DIRECTION('ref_axis',(1.,0.,0.));
#19969=DIRECTION('center_axis',(0.,1.,0.));
#19970=DIRECTION('ref_axis',(1.,0.,0.));
#19971=DIRECTION('center_axis',(0.,1.,0.));
#19972=DIRECTION('ref_axis',(1.,0.,0.));
#19973=DIRECTION('',(0.,-1.,0.));
#19974=DIRECTION('center_axis',(0.,1.,0.));
#19975=DIRECTION('ref_axis',(1.,0.,0.));
#19976=DIRECTION('center_axis',(0.,1.,0.));
#19977=DIRECTION('ref_axis',(1.,0.,0.));
#19978=DIRECTION('center_axis',(0.,1.,0.));
#19979=DIRECTION('ref_axis',(1.,0.,0.));
#23959=CARTESIAN_POINT('',(0.,0.,0.));
#23960=CARTESIAN_POINT('Origin',(38.7298334620742,7.,3.));
#23961=CARTESIAN_POINT('',(38.1248334620742,8.,3.));
#23962=CARTESIAN_POINT('Origin',(38.7298334620742,8.,3.));
#23963=CARTESIAN_POINT('',(38.1248334620742,7.,3.));
#23964=CARTESIAN_POINT('',(38.1248334620742,7.,3.));
#23965=CARTESIAN_POINT('Origin',(38.7298334620742,7.,3.));
#23966=CARTESIAN_POINT('Origin',(38.7298334620742,7.,3.));
#23967=CARTESIAN_POINT('',(37.7298334620742,8.,3.));
#23968=CARTESIAN_POINT('Origin',(38.7298334620742,8.,3.));
#23969=CARTESIAN_POINT('',(37.7298334620742,7.,3.));
#23970=CARTESIAN_POINT('',(37.7298334620742,7.,3.));
#23971=CARTESIAN_POINT('Origin',(38.7298334620742,7.,3.));
#23972=CARTESIAN_POINT('Origin',(38.7298334620742,8.,3.));
#23973=CARTESIAN_POINT('Origin',(38.7298334620742,7.,3.));
#24954=UNCERTAINTY_MEASURE_WITH_UNIT(LENGTH_MEASURE(0.001),#25101,
'DISTANCE_ACCURACY_VALUE',
'Maximum model space distance between geometric entities at asserted c
onnectivities');
#24979=UNCERTAINTY_MEASURE_WITH_UNIT(LENGTH_MEASURE(0.001),#25101,
'DISTANCE_ACCURACY_VALUE',
'Maximum model space distance between geometric entities at asserted c
onnectivities');
#25075=(
GEOMETRIC_REPRESENTATION_CONTEXT(3)
GLOBAL_UNCERTAINTY_ASSIGNED_CONTEXT((#24954))
GLOBAL_UNIT_ASSIGNED_CONTEXT((#25101,#25103,#25104))
REPRESENTATION_CONTEXT('','3D')
);
#25100=(
GEOMETRIC_REPRESENTATION_CONTEXT(3)
GLOBAL_UNCERTAINTY_ASSIGNED_CONTEXT((#24979))
GLOBAL_UNIT_ASSIGNED_CONTEXT((#25101,#25103,#25104))
REPRESENTATION_CONTEXT('','3D')
);
#25101=(
LENGTH_UNIT()
NAMED_UNIT(*)
SI_UNIT(.CENTI.,.METRE.)
);
#25103=(
NAMED_UNIT(*)
PLANE_ANGLE_UNIT()
SI_UNIT($,.RADIAN.)
);
#25104=(
NAMED_UNIT(*)
SI_UNIT($,.STERADIAN.)
SOLID_ANGLE_UNIT()
);
#25200=SHAPE_DEFINITION_REPRESENTATION(#25394,#25605);
#25394=PRODUCT_DEFINITION_SHAPE('',$,#25726);
#25605=SHAPE_REPRESENTATION('',(#15992),#25075);
#25630=PRODUCT_DEFINITION_CONTEXT('part definition',#25992,'design');
#25726=PRODUCT_DEFINITION('Plain pivot bush (8)','Plain pivot bush (8)',#25846,
#25630);
#25846=PRODUCT_DEFINITION_FORMATION('',$,#26089);
#25992=APPLICATION_CONTEXT(
'Core Data for Automotive Mechanical Design Process');
#25993=PRODUCT_CONTEXT('part definition',#25992,'mechanical');
#26089=PRODUCT('Plain pivot bush (8)','Plain pivot bush (8)',
'Plain pivot bush (8)',(#25993));
#26171=COLOUR_RGB('Light Blue',0.38,0.62,0.78);
#26172=FILL_AREA_STYLE_COLOUR('',#26171);
#26173=FILL_AREA_STYLE('',(#26172));
#26174=SURFACE_STYLE_FILL_AREA(#26173);
#26175=SURFACE_SIDE_STYLE('',(#26174));
#26176=SURFACE_STYLE_USAGE(.BOTH.,#26175);
#26177=PRESENTATION_STYLE_ASSIGNMENT((#26176));
ENDSEC;
END-ISO-10303-21;
